ISO-10303-21;
HEADER;
FILE_DESCRIPTION (('STEP AP214'),
    '1' );
FILE_NAME ( 'ISO 4762 M5x16 Socket Head Cap Screw.step', '2026-10-06T08:24:41', ( '' ), ( '' ), 'STEP AP214', 'Unspecified', '' );
FILE_SCHEMA (( 'AUTOMOTIVE_DESIGN' ));
ENDSEC;
DATA;
#23=EDGE_CURVE ( 'NONE', #19722, #14586, #4579, .T. ) ;
#203=ADVANCED_FACE ( 'NONE', ( #17324 ), #15936, .F. ) ;
#207=ORIENTED_EDGE ( 'NONE', *, *, #6942, .F. ) ;
#375=DIRECTION ( 'NONE',  ( -0.5000000010362850578, -0.8660254031861391866, -1.060575237992201443E-16 ) ) ;
#383=EDGE_CURVE ( 'NONE', #23520, #15671, #17764, .T. ) ;
#440=EDGE_CURVE ( 'NONE', #19589, #20556, #3761, .T. ) ;
#472=AXIS2_PLACEMENT_3D ( 'NONE', #24555, #16101, #700 ) ;
#476=CARTESIAN_POINT ( 'NONE',  ( -0.1968503937007874127, -0.07874015748031495954, 0.04546065111729338803 ) ) ;
#569=DIRECTION ( 'NONE',  ( -7.017815000000000124E-18, 1.000000000000000000, -1.224646799147353207E-16 ) ) ;
#616=DIRECTION ( 'NONE',  ( 0.000000000000000000, 0.000000000000000000, 1.000000000000000000 ) ) ;
#632=DIRECTION ( 'NONE',  ( 1.000000000000000000, 0.000000000000000000, 0.000000000000000000 ) ) ;
#643=AXIS2_PLACEMENT_3D ( 'NONE', #12530, #2842, #19821 ) ;
#650=( CONVERSION_BASED_UNIT ( 'INCH', #22538 ) LENGTH_UNIT ( ) NAMED_UNIT ( #5813 ) ) ;
#655=ORIENTED_EDGE ( 'NONE', *, *, #26490, .T. ) ;
#680=CARTESIAN_POINT ( 'NONE',  ( -0.1968503937007874127, -0.07874015748031495954, -0.04546065111729331171 ) ) ;
#700=DIRECTION ( 'NONE',  ( 0.000000000000000000, -1.000000000000000000, 0.000000000000000000 ) ) ;
#830=VERTEX_POINT ( 'NONE', #16815 ) ;
#868=EDGE_CURVE ( 'NONE', #18194, #14499, #21744, .T. ) ;
#930=ORIENTED_EDGE ( 'NONE', *, *, #14908, .T. ) ;
#934=ADVANCED_FACE ( 'NONE', ( #12702 ), #12572, .T. ) ;
#976=AXIS2_PLACEMENT_3D ( 'NONE', #6874, #2210, #8577 ) ;
#1058=CARTESIAN_POINT ( 'NONE',  ( 0.3543307086614173040, 0.09842519685039370636, 0.000000000000000000 ) ) ;
#1078=EDGE_CURVE ( 'NONE', #21206, #27702, #25930, .T. ) ;
#1133=AXIS2_PLACEMENT_3D ( 'NONE', #26214, #24367, #4873 ) ;
#1157=ORIENTED_EDGE ( 'NONE', *, *, #4766, .T. ) ;
#1197=FACE_OUTER_BOUND ( 'NONE', #10306, .T. ) ;
#1383=ORIENTED_EDGE ( 'NONE', *, *, #9079, .F. ) ;
#1387=ORIENTED_EDGE ( 'NONE', *, *, #868, .F. ) ;
#1391=EDGE_LOOP ( 'NONE', ( #10847, #9059, #13103, #2091, #25323 ) ) ;
#1400=UNCERTAINTY_MEASURE_WITH_UNIT (LENGTH_MEASURE( 1.000000000000000082E-05 ), #650, 'distance_accuracy_value', 'NONE') ;
#1446=CIRCLE ( 'NONE', #16780, 0.1673228346456692994 ) ;
#1471=EDGE_CURVE ( 'NONE', #15671, #13676, #13355, .T. ) ;
#1486=AXIS2_PLACEMENT_3D ( 'NONE', #9366, #24771, #24355 ) ;
#1504=CARTESIAN_POINT ( 'NONE',  ( -0.09842519685039370636, -0.07874015748031495954, 0.04546065111729338803 ) ) ;
#1558=DIRECTION ( 'NONE',  ( 3.508908000000000588E-18, -0.4999999999999998890, -0.8660254037844388186 ) ) ;
#1568=ADVANCED_FACE ( 'NONE', ( #2880 ), #4596, .F. ) ;
#1569=DIRECTION ( 'NONE',  ( 0.000000000000000000, -1.000000000000000000, 0.000000000000000000 ) ) ;
#1681=( GEOMETRIC_REPRESENTATION_CONTEXT ( 3 ) GLOBAL_UNCERTAINTY_ASSIGNED_CONTEXT ( ( #1400 ) ) GLOBAL_UNIT_ASSIGNED_CONTEXT ( ( #650, #19998, #2884 ) ) REPRESENTATION_CONTEXT ( 'NONE', 'WORKASPACE' ) ) ;
#1717=DIRECTION ( 'NONE',  ( -1.000000000000000000, 0.000000000000000000, 0.000000000000000000 ) ) ;
#1747=DIRECTION ( 'NONE',  ( 0.000000000000000000, -1.000000000000000000, 0.000000000000000000 ) ) ;
#1750=UNCERTAINTY_MEASURE_WITH_UNIT (LENGTH_MEASURE( 1.000000000000000082E-05 ), #8720, 'distance_accuracy_value', 'NONE') ;
#1866=CARTESIAN_POINT ( 'NONE',  ( 0.003937007874015826907, -4.393043307086613241E-18, 0.000000000000000000 ) ) ;
#2004=DIRECTION ( 'NONE',  ( -0.000000000000000000, 1.000000000000000000, 0.000000000000000000 ) ) ;
#2091=ORIENTED_EDGE ( 'NONE', *, *, #2318, .F. ) ;
#2141=EDGE_CURVE ( 'NONE', #20556, #17614, #19275, .T. ) ;
#2196=DIRECTION ( 'NONE',  ( 1.000000000000000000, 0.000000000000000000, 0.000000000000000000 ) ) ;
#2210=DIRECTION ( 'NONE',  ( 7.017815000000000124E-18, -1.000000000000000000, 0.000000000000000000 ) ) ;
#2220=( LENGTH_UNIT ( ) NAMED_UNIT ( * ) SI_UNIT ( $, .METRE. ) ) ;
#2318=EDGE_CURVE ( 'NONE', #17614, #17378, #8133, .T. ) ;
#2378=PRODUCT_DEFINITION ( 'UNKNOWN', '', #3426, #24918 ) ;
#2425=AXIS2_PLACEMENT_3D ( 'NONE', #1866, #4132, #17396 ) ;
#2502=ORIENTED_EDGE ( 'NONE', *, *, #15206, .T. ) ;
#2520=VECTOR ( 'NONE', #6987, 39.37007874015748143 ) ;
#2608=CIRCLE ( 'NONE', #7135, 0.09842519685039370636 ) ;
#2619=EDGE_LOOP ( 'NONE', ( #16072, #19591, #4603, #3997 ) ) ;
#2699=CARTESIAN_POINT ( 'NONE',  ( -0.09842519685039370636, -1.570035826771653483E-17, -0.09092130223458683158 ) ) ;
#2710=CARTESIAN_POINT ( 'NONE',  ( -0.1968503937007874127, 0.07874015748031495954, -0.04546065111729338803 ) ) ;
#2719=CARTESIAN_POINT ( 'NONE',  ( -0.09842519685039370636, 2.800920866141732248E-17, 0.09092130223458683158 ) ) ;
#2762=ORIENTED_EDGE ( 'NONE', *, *, #8060, .F. ) ;
#2774=DIRECTION ( 'NONE',  ( 0.000000000000000000, 0.000000000000000000, -1.000000000000000000 ) ) ;
#2840=AXIS2_PLACEMENT_3D ( 'NONE', #15686, #7071, #20057 ) ;
#2842=DIRECTION ( 'NONE',  ( -1.000000000000000000, 0.000000000000000000, 0.000000000000000000 ) ) ;
#2873=PRODUCT_CONTEXT ( 'NONE', #22595, 'mechanical' ) ;
#2880=FACE_OUTER_BOUND ( 'NONE', #3212, .T. ) ;
#2884=( NAMED_UNIT ( * ) SI_UNIT ( $, .STERADIAN. ) SOLID_ANGLE_UNIT ( ) ) ;
#2945=FACE_OUTER_BOUND ( 'NONE', #13500, .T. ) ;
#2967=DIRECTION ( 'NONE',  ( 0.000000000000000000, -1.000000000000000000, 0.000000000000000000 ) ) ;
#2993=( BOUNDED_CURVE ( )  B_SPLINE_CURVE ( 2, ( #2719, #11082, #17834 ),
 .UNSPECIFIED., .F., .T. ) 
 B_SPLINE_CURVE_WITH_KNOTS ( ( 3, 3 ),
 ( 0.000000000000000000, 0.2336872276155829986 ),
 .UNSPECIFIED. ) 
 CURVE ( )  GEOMETRIC_REPRESENTATION_ITEM ( )  RATIONAL_B_SPLINE_CURVE ( ( 1.000000000000000000, 1.154700538379249908, 1.000000000000000000 ) ) 
 REPRESENTATION_ITEM ( '' )  ) ;
#3018=( LENGTH_UNIT ( ) NAMED_UNIT ( * ) SI_UNIT ( $, .METRE. ) ) ;
#3061=DIRECTION ( 'NONE',  ( 0.000000000000000000, 1.000000000000000000, 0.000000000000000000 ) ) ;
#3134=LENGTH_MEASURE_WITH_UNIT ( LENGTH_MEASURE( 0.02539999999999999897 ), #2220 ) ;
#3212=EDGE_LOOP ( 'NONE', ( #10838, #26594, #26632, #8189 ) ) ;
#3230=DIRECTION ( 'NONE',  ( 0.000000000000000000, -0.8660254037844388186, 0.4999999999999998890 ) ) ;
#3234=CARTESIAN_POINT ( 'NONE',  ( -0.08530183727034115759, -0.03937007874015747977, 0.06819097667594049839 ) ) ;
#3340=ORIENTED_EDGE ( 'NONE', *, *, #4961, .F. ) ;
#3373=CARTESIAN_POINT ( 'NONE',  ( 8.741913385826771462E-17, 0.1673228346456692994, 0.000000000000000000 ) ) ;
#3426=PRODUCT_DEFINITION_FORMATION_WITH_SPECIFIED_SOURCE ( 'ANY', '', #16553, .NOT_KNOWN. ) ;
#3473=( GEOMETRIC_REPRESENTATION_CONTEXT ( 3 ) GLOBAL_UNCERTAINTY_ASSIGNED_CONTEXT ( ( #1750 ) ) GLOBAL_UNIT_ASSIGNED_CONTEXT ( ( #8720, #22365, #26090 ) ) REPRESENTATION_CONTEXT ( 'NONE', 'WORKASPACE' ) ) ;
#3521=CARTESIAN_POINT ( 'NONE',  ( -0.09139240964747702423, 0.07874015748031500117, -1.981023540891279271E-18 ) ) ;
#3562=LINE ( 'NONE', #14482, #21706 ) ;
#3626=EDGE_CURVE ( 'NONE', #27013, #12986, #15457, .T. ) ;
#3665=DIRECTION ( 'NONE',  ( 0.000000000000000000, 0.000000000000000000, 1.000000000000000000 ) ) ;
#3710=EDGE_CURVE ( 'NONE', #14499, #7850, #8799, .T. ) ;
#3723=CARTESIAN_POINT ( 'NONE',  ( -0.1968503937007874127, -5.802129921259842692E-18, 0.000000000000000000 ) ) ;
#3761=( BOUNDED_CURVE ( )  B_SPLINE_CURVE ( 2, ( #8910, #12735, #11040 ),
 .UNSPECIFIED., .F., .T. ) 
 B_SPLINE_CURVE_WITH_KNOTS ( ( 3, 3 ),
 ( 0.000000000000000000, 0.1168436138077912356 ),
 .UNSPECIFIED. ) 
 CURVE ( )  GEOMETRIC_REPRESENTATION_ITEM ( )  RATIONAL_B_SPLINE_CURVE ( ( 1.000000000000000000, 1.077350269189625731, 1.077350269189625953 ) ) 
 REPRESENTATION_ITEM ( '' )  ) ;
#3813=DIRECTION ( 'NONE',  ( 0.000000000000000000, -0.8660254037844385966, 0.4999999999999998335 ) ) ;
#3858=ORIENTED_EDGE ( 'NONE', *, *, #25706, .T. ) ;
#3952=CARTESIAN_POINT ( 'NONE',  ( -0.09842519685039370636, -0.07874015748031495954, -0.04546065111729338803 ) ) ;
#3955=DIRECTION ( 'NONE',  ( -1.000000000000000000, 0.000000000000000000, 0.000000000000000000 ) ) ;
#3997=ORIENTED_EDGE ( 'NONE', *, *, #24206, .F. ) ;
#4002=CARTESIAN_POINT ( 'NONE',  ( -0.09842519685039370636, -1.570035826771653483E-17, -0.09092130223458683158 ) ) ;
#4054=DIRECTION ( 'NONE',  ( -1.000000000000000000, 0.000000000000000000, 0.000000000000000000 ) ) ;
#4078=VERTEX_POINT ( 'NONE', #20590 ) ;
#4098=LINE ( 'NONE', #19058, #17352 ) ;
#4132=DIRECTION ( 'NONE',  ( -1.000000000000000000, 0.000000000000000000, 0.000000000000000000 ) ) ;
#4216=EDGE_LOOP ( 'NONE', ( #13398, #18115 ) ) ;
#4332=EDGE_LOOP ( 'NONE', ( #27446, #6202 ) ) ;
#4360=PLANE ( 'NONE',  #20753 ) ;
#4411=PLANE ( 'NONE',  #21842 ) ;
#4432=LINE ( 'NONE', #19684, #10993 ) ;
#4473=CARTESIAN_POINT ( 'NONE',  ( -0.07217847769028858107, -4.927204724409449161E-18, 0.000000000000000000 ) ) ;
#4540=DIRECTION ( 'NONE',  ( -1.000000000000000000, 0.000000000000000000, 0.000000000000000000 ) ) ;
#4550=CARTESIAN_POINT ( 'NONE',  ( -0.09139240964747710749, -0.07874015748031500117, -1.188614124534770567E-17 ) ) ;
#4579=LINE ( 'NONE', #17578, #6039 ) ;
#4596=PLANE ( 'NONE',  #1133 ) ;
#4603=ORIENTED_EDGE ( 'NONE', *, *, #19074, .F. ) ;
#4641=ORIENTED_EDGE ( 'NONE', *, *, #23, .T. ) ;
#4724=DIRECTION ( 'NONE',  ( 0.000000000000000000, 0.000000000000000000, -1.000000000000000000 ) ) ;
#4760=ORIENTED_EDGE ( 'NONE', *, *, #9446, .F. ) ;
#4766=EDGE_CURVE ( 'NONE', #21315, #23520, #2608, .T. ) ;
#4807=ADVANCED_FACE ( 'NONE', ( #17392 ), #18382, .T. ) ;
#4822=( BOUNDED_CURVE ( )  B_SPLINE_CURVE ( 2, ( #2699, #15333, #6692 ),
 .UNSPECIFIED., .F., .T. ) 
 B_SPLINE_CURVE_WITH_KNOTS ( ( 3, 3 ),
 ( 0.000000000000000000, 0.2336872276155829986 ),
 .UNSPECIFIED. ) 
 CURVE ( )  GEOMETRIC_REPRESENTATION_ITEM ( )  RATIONAL_B_SPLINE_CURVE ( ( 1.000000000000000000, 1.154700538379245911, 1.000000000000000000 ) ) 
 REPRESENTATION_ITEM ( '' )  ) ;
#4836=LINE ( 'NONE', #2710, #19818 ) ;
#4837=ADVANCED_FACE ( 'NONE', ( #16350 ), #9841, .F. ) ;
#4873=DIRECTION ( 'NONE',  ( 1.000000000000000000, 7.017815999999999636E-18, 0.000000000000000000 ) ) ;
#4961=EDGE_CURVE ( 'NONE', #7941, #21315, #21587, .T. ) ;
#4969=EDGE_LOOP ( 'NONE', ( #8615, #8882, #20950, #23233 ) ) ;
#5051=ORIENTED_EDGE ( 'NONE', *, *, #20893, .F. ) ;
#5095=AXIS2_PLACEMENT_3D ( 'NONE', #4473, #9480, #20093 ) ;
#5175=DIRECTION ( 'NONE',  ( -1.000000000000000000, 0.000000000000000000, 0.000000000000000000 ) ) ;
#5201=ORIENTED_EDGE ( 'NONE', *, *, #17489, .T. ) ;
#5211=DIRECTION ( 'NONE',  ( 0.000000000000000000, 1.224646799147355919E-16, 1.000000000000000000 ) ) ;
#5229=CARTESIAN_POINT ( 'NONE',  ( 0.000000000000000000, 0.000000000000000000, 0.000000000000000000 ) ) ;
#5247=ORIENTED_EDGE ( 'NONE', *, *, #19961, .T. ) ;
#5256=AXIS2_PLACEMENT_3D ( 'NONE', #11090, #632, #24081 ) ;
#5299=SURFACE_SIDE_STYLE ('',( #18275 ) ) ;
#5340=CARTESIAN_POINT ( 'NONE',  ( -0.09139240964747702423, 0.07874015748031500117, -1.981023540891279271E-18 ) ) ;
#5433=ADVANCED_FACE ( 'NONE', ( #7173 ), #21880, .F. ) ;
#5484=APPLICATION_CONTEXT ( 'automotive_design' ) ;
#5495=FACE_OUTER_BOUND ( 'NONE', #9560, .T. ) ;
#5534=CARTESIAN_POINT ( 'NONE',  ( -0.1968503937007874127, -0.07874015748031495954, 0.04546065111729338803 ) ) ;
#5584=DIRECTION ( 'NONE',  ( 0.000000000000000000, 0.000000000000000000, -1.000000000000000000 ) ) ;
#5612=CIRCLE ( 'NONE', #14189, 0.07910393700787400617 ) ;
#5676=AXIS2_PLACEMENT_3D ( 'NONE', #21516, #25751, #21784 ) ;
#5694=EDGE_CURVE ( 'NONE', #17378, #25403, #4836, .T. ) ;
#5765=EDGE_LOOP ( 'NONE', ( #6628, #2502, #24974, #21666, #6750, #20699 ) ) ;
#5811=CARTESIAN_POINT ( 'NONE',  ( -0.09842519685039370636, 2.800920866141732248E-17, 0.09092130223458683158 ) ) ;
#5813=DIMENSIONAL_EXPONENTS ( 1.000000000000000000, 0.000000000000000000, 0.000000000000000000, 0.000000000000000000, 0.000000000000000000, 0.000000000000000000, 0.000000000000000000 ) ;
#5837=ORIENTED_EDGE ( 'NONE', *, *, #19961, .F. ) ;
#5952=EDGE_CURVE ( 'NONE', #19912, #830, #4822, .T. ) ;
#6039=VECTOR ( 'NONE', #26191, 39.37007874015748854 ) ;
#6074=ORIENTED_EDGE ( 'NONE', *, *, #8060, .T. ) ;
#6202=ORIENTED_EDGE ( 'NONE', *, *, #17489, .F. ) ;
#6263=DIRECTION ( 'NONE',  ( -1.000000000000000000, 0.000000000000000000, 0.000000000000000000 ) ) ;
#6447=EDGE_CURVE ( 'NONE', #19912, #4078, #8564, .T. ) ;
#6466=EDGE_LOOP ( 'NONE', ( #19788, #21058, #3858, #5051, #27315 ) ) ;
#6499=ORIENTED_EDGE ( 'NONE', *, *, #21788, .F. ) ;
#6510=ORIENTED_EDGE ( 'NONE', *, *, #8464, .T. ) ;
#6519=DIRECTION ( 'NONE',  ( 1.000000000000000000, 0.000000000000000000, 0.000000000000000000 ) ) ;
#6555=DIRECTION ( 'NONE',  ( 1.000000000000000000, 0.000000000000000000, 0.000000000000000000 ) ) ;
#6628=ORIENTED_EDGE ( 'NONE', *, *, #5694, .T. ) ;
#6667=CARTESIAN_POINT ( 'NONE',  ( -0.1968503937007874127, -5.733057234251967840E-18, -0.1476377952755905387 ) ) ;
#6677=CARTESIAN_POINT ( 'NONE',  ( -0.09139240964747707974, -0.07874015748031501505, -0.02109836160874977232 ) ) ;
#6692=CARTESIAN_POINT ( 'NONE',  ( -0.09842519685039370636, -0.07874015748031495954, -0.04546065111729338803 ) ) ;
#6701=AXIS2_PLACEMENT_3D ( 'NONE', #26793, #26647, #13658 ) ;
#6737=DIRECTION ( 'NONE',  ( 1.000000000000000000, 0.000000000000000000, 0.000000000000000000 ) ) ;
#6750=ORIENTED_EDGE ( 'NONE', *, *, #19074, .T. ) ;
#6762=CARTESIAN_POINT ( 'NONE',  ( 8.741913385826771462E-17, 0.1328740157480315098, 0.000000000000000000 ) ) ;
#6770=EDGE_CURVE ( 'NONE', #27702, #14224, #23023, .T. ) ;
#6807=ORIENTED_EDGE ( 'NONE', *, *, #14443, .F. ) ;
#6856=CARTESIAN_POINT ( 'NONE',  ( 0.003937007874015826907, 7.887824528841537495E-18, 0.09842519685039370636 ) ) ;
#6874=CARTESIAN_POINT ( 'NONE',  ( -0.1771653543307086520, -5.663984251968503442E-18, -0.1476377952755905387 ) ) ;
#6942=EDGE_CURVE ( 'NONE', #19742, #13676, #16508, .T. ) ;
#6987=DIRECTION ( 'NONE',  ( 1.000000000000000000, 0.000000000000000000, 0.000000000000000000 ) ) ;
#7071=DIRECTION ( 'NONE',  ( 1.000000000000000000, 0.000000000000000000, 0.000000000000000000 ) ) ;
#7085=ADVANCED_FACE ( 'NONE', ( #13245, #23864 ), #4360, .T. ) ;
#7122=DIRECTION ( 'NONE',  ( 1.000000000000000000, 7.017815000000030939E-18, 0.000000000000000000 ) ) ;
#7135=AXIS2_PLACEMENT_3D ( 'NONE', #17256, #25596, #19660 ) ;
#7173=FACE_OUTER_BOUND ( 'NONE', #25395, .T. ) ;
#7191=VERTEX_POINT ( 'NONE', #10853 ) ;
#7290=EDGE_LOOP ( 'NONE', ( #6807, #8826, #25513, #2762, #3340 ) ) ;
#7400=DIRECTION ( 'NONE',  ( 0.000000000000000000, 0.000000000000000000, -1.000000000000000000 ) ) ;
#7469=ORIENTED_EDGE ( 'NONE', *, *, #4961, .T. ) ;
#7500=ORIENTED_EDGE ( 'NONE', *, *, #26466, .F. ) ;
#7504=CIRCLE ( 'NONE', #11550, 0.09842519685039370636 ) ;
#7533=DIRECTION ( 'NONE',  ( 0.000000000000000000, 0.000000000000000000, -1.000000000000000000 ) ) ;
#7652=PLANE ( 'NONE',  #12275 ) ;
#7661=ADVANCED_FACE ( 'NONE', ( #27645 ), #15208, .T. ) ;
#7696=DIRECTION ( 'NONE',  ( -1.000000000000000000, 0.000000000000000000, 0.000000000000000000 ) ) ;
#7792=CIRCLE ( 'NONE', #8257, 0.07910393700787400617 ) ;
#7850=VERTEX_POINT ( 'NONE', #24083 ) ;
#7923=DIRECTION ( 'NONE',  ( 1.000000000000000000, 0.000000000000000000, 0.000000000000000000 ) ) ;
#7938=FACE_OUTER_BOUND ( 'NONE', #7290, .T. ) ;
#7941=VERTEX_POINT ( 'NONE', #6856 ) ;
#7954=EDGE_CURVE ( 'NONE', #27013, #14499, #3562, .T. ) ;
#8060=EDGE_CURVE ( 'NONE', #21315, #14586, #27045, .T. ) ;
#8133=LINE ( 'NONE', #21122, #17835 ) ;
#8189=ORIENTED_EDGE ( 'NONE', *, *, #26368, .F. ) ;
#8197=CARTESIAN_POINT ( 'NONE',  ( -0.09842519685039370636, -5.111401574803149519E-18, 0.000000000000000000 ) ) ;
#8257=AXIS2_PLACEMENT_3D ( 'NONE', #12312, #1717, #12461 ) ;
#8417=CIRCLE ( 'NONE', #5256, 0.1023622047244094474 ) ;
#8464=EDGE_CURVE ( 'NONE', #20489, #11946, #1446, .T. ) ;
#8493=AXIS2_PLACEMENT_3D ( 'NONE', #15298, #4540, #17529 ) ;
#8564=LINE ( 'NONE', #10248, #16240 ) ;
#8577=DIRECTION ( 'NONE',  ( 1.000000000000000000, 7.017814999999989339E-18, 0.000000000000000000 ) ) ;
#8615=ORIENTED_EDGE ( 'NONE', *, *, #26620, .F. ) ;
#8626=CARTESIAN_POINT ( 'NONE',  ( -0.09842519685039370636, 0.07874015748031495954, -0.04546065111729338803 ) ) ;
#8680=LINE ( 'NONE', #19420, #2520 ) ;
#8697=FACE_OUTER_BOUND ( 'NONE', #20863, .T. ) ;
#8718=ORIENTED_EDGE ( 'NONE', *, *, #15227, .F. ) ;
#8720=( CONVERSION_BASED_UNIT ( 'INCH', #3134 ) LENGTH_UNIT ( ) NAMED_UNIT ( #24789 ) ) ;
#8747=ADVANCED_FACE ( 'NONE', ( #12453 ), #7652, .F. ) ;
#8766=AXIS2_PLACEMENT_3D ( 'NONE', #8197, #21335, #10578 ) ;
#8789=CARTESIAN_POINT ( 'NONE',  ( 0.003937007874015826907, 0.09842519685039370636, 0.000000000000000000 ) ) ;
#8799=LINE ( 'NONE', #476, #17546 ) ;
#8823=CARTESIAN_POINT ( 'NONE',  ( 0.003937007874015826907, -4.393043307086613241E-18, -0.1023622047244094474 ) ) ;
#8826=ORIENTED_EDGE ( 'NONE', *, *, #1471, .T. ) ;
#8882=ORIENTED_EDGE ( 'NONE', *, *, #868, .T. ) ;
#8903=CARTESIAN_POINT ( 'NONE',  ( -0.1968503937007874127, 1.355271913027328057E-17, 0.1476377952755905387 ) ) ;
#8910=CARTESIAN_POINT ( 'NONE',  ( -0.09842519685039370636, 0.07874015748031495954, 0.04546065111729331171 ) ) ;
#8918=CARTESIAN_POINT ( 'NONE',  ( -0.09139240964747707974, -0.07874015748031502893, 0.02109836160874977232 ) ) ;
#8979=ORIENTED_EDGE ( 'NONE', *, *, #20893, .T. ) ;
#9021=VECTOR ( 'NONE', #22881, 39.37007874015748854 ) ;
#9059=ORIENTED_EDGE ( 'NONE', *, *, #26368, .T. ) ;
#9079=EDGE_CURVE ( 'NONE', #7941, #17590, #25838, .T. ) ;
#9094=DIRECTION ( 'NONE',  ( 0.000000000000000000, 1.000000000000000000, 0.000000000000000000 ) ) ;
#9188=SHAPE_REPRESENTATION ( 'ISO 4762 M5x16 Socket Head Cap Screw', ( #11588, #27978, #27991, #28004 ), #3473 ) ;
#9345=ADVANCED_FACE ( 'NONE', ( #13205 ), #11222, .T. ) ;
#9366=CARTESIAN_POINT ( 'NONE',  ( 8.741913385826771462E-17, -4.420669291338583154E-18, 0.000000000000000000 ) ) ;
#9376=CARTESIAN_POINT ( 'NONE',  ( 0.3543307086614173040, -0.09842519685039370636, 1.205361022782828035E-17 ) ) ;
#9391=AXIS2_PLACEMENT_3D ( 'NONE', #680, #17883, #2774 ) ;
#9446=EDGE_CURVE ( 'NONE', #11946, #20489, #12313, .T. ) ;
#9464=ORIENTED_EDGE ( 'NONE', *, *, #11700, .T. ) ;
#9480=DIRECTION ( 'NONE',  ( -1.000000000000000000, 0.000000000000000000, 0.000000000000000000 ) ) ;
#9502=CARTESIAN_POINT ( 'NONE',  ( 0.003937007874015826907, -4.393043307086613241E-18, 0.000000000000000000 ) ) ;
#9560=EDGE_LOOP ( 'NONE', ( #16017, #9464, #14779, #25368, #20740, #15992 ) ) ;
#9584=EDGE_CURVE ( 'NONE', #13641, #25766, #23613, .T. ) ;
#9650=LINE ( 'NONE', #16436, #14639 ) ;
#9675=FILL_AREA_STYLE_COLOUR ( '', #17021 ) ;
#9698=( BOUNDED_CURVE ( )  B_SPLINE_CURVE ( 2, ( #26159, #8918, #24037 ),
 .UNSPECIFIED., .F., .T. ) 
 B_SPLINE_CURVE_WITH_KNOTS ( ( 3, 3 ),
 ( 0.1168436138077914160, 0.2336872276155829709 ),
 .UNSPECIFIED. ) 
 CURVE ( )  GEOMETRIC_REPRESENTATION_ITEM ( )  RATIONAL_B_SPLINE_CURVE ( ( 1.077350269189623067, 1.077350269189623067, 1.000000000000000000 ) ) 
 REPRESENTATION_ITEM ( '' )  ) ;
#9716=ORIENTED_EDGE ( 'NONE', *, *, #2318, .T. ) ;
#9737=CONICAL_SURFACE ( 'NONE', #5676, 0.08876456692913387014, 0.7853981624999977207 ) ;
#9762=CARTESIAN_POINT ( 'NONE',  ( -0.1771653543307086520, -5.663984251968503442E-18, 0.000000000000000000 ) ) ;
#9772=DIRECTION ( 'NONE',  ( 0.000000000000000000, -1.000000000000000000, 0.000000000000000000 ) ) ;
#9782=MECHANICAL_DESIGN_GEOMETRIC_PRESENTATION_REPRESENTATION('',(#27853),#1681);
#9812=ORIENTED_EDGE ( 'NONE', *, *, #27335, .T. ) ;
#9841=PLANE ( 'NONE',  #6701 ) ;
#9857=EDGE_CURVE ( 'NONE', #14224, #11946, #4432, .T. ) ;
#9861=DIRECTION ( 'NONE',  ( -1.000000000000000000, 0.000000000000000000, 0.000000000000000000 ) ) ;
#9923=CARTESIAN_POINT ( 'NONE',  ( -0.1771653543307086520, -5.663984251968503442E-18, 0.000000000000000000 ) ) ;
#9933=DIRECTION ( 'NONE',  ( 0.000000000000000000, 0.8660254037844385966, 0.4999999999999998335 ) ) ;
#9936=DIRECTION ( 'NONE',  ( 0.000000000000000000, -0.8660254037844385966, -0.4999999999999998335 ) ) ;
#10009=ORIENTED_EDGE ( 'NONE', *, *, #19680, .T. ) ;
#10017=EDGE_CURVE ( 'NONE', #14224, #13094, #11419, .T. ) ;
#10142=ORIENTED_EDGE ( 'NONE', *, *, #9857, .T. ) ;
#10180=ADVANCED_FACE ( 'NONE', ( #7938 ), #27577, .T. ) ;
#10248=CARTESIAN_POINT ( 'NONE',  ( -0.09842519685039370636, 5.809059055118109875E-18, -0.09092130223458683158 ) ) ;
#10306=EDGE_LOOP ( 'NONE', ( #1383, #7469, #1157, #8979, #9812 ) ) ;
#10377=CARTESIAN_POINT ( 'NONE',  ( -0.09842519685039370636, 0.07874015748031495954, 0.04546065111729331171 ) ) ;
#10392=( BOUNDED_CURVE ( )  B_SPLINE_CURVE ( 2, ( #19344, #21192, #23036 ),
 .UNSPECIFIED., .F., .T. ) 
 B_SPLINE_CURVE_WITH_KNOTS ( ( 3, 3 ),
 ( 0.000000000000000000, 0.2336872276155829986 ),
 .UNSPECIFIED. ) 
 CURVE ( )  GEOMETRIC_REPRESENTATION_ITEM ( )  RATIONAL_B_SPLINE_CURVE ( ( 1.000000000000000000, 1.154700538379251906, 1.000000000000000000 ) ) 
 REPRESENTATION_ITEM ( '' )  ) ;
#10490=CARTESIAN_POINT ( 'NONE',  ( 8.741913385826771462E-17, -4.420669291338583154E-18, 0.000000000000000000 ) ) ;
#10578=DIRECTION ( 'NONE',  ( 0.000000000000000000, 1.000000000000000000, 0.000000000000000000 ) ) ;
#10584=AXIS2_PLACEMENT_3D ( 'NONE', #12930, #17716, #4724 ) ;
#10750=AXIS2_PLACEMENT_3D ( 'NONE', #11431, #20333, #26824 ) ;
#10764=EDGE_LOOP ( 'NONE', ( #6510, #12950 ) ) ;
#10835=ORIENTED_EDGE ( 'NONE', *, *, #9584, .T. ) ;
#10838=ORIENTED_EDGE ( 'NONE', *, *, #10995, .F. ) ;
#10847=ORIENTED_EDGE ( 'NONE', *, *, #440, .F. ) ;
#10853=CARTESIAN_POINT ( 'NONE',  ( -0.09139240964747710749, -0.07874015748031500117, -1.188614124534770567E-17 ) ) ;
#10871=CARTESIAN_POINT ( 'NONE',  ( -0.1968503937007874127, -0.07874015748031495954, -0.04546065111729338803 ) ) ;
#10993=VECTOR ( 'NONE', #21665, 39.37007874015748143 ) ;
#10995=EDGE_CURVE ( 'NONE', #12986, #19589, #2993, .T. ) ;
#11040=CARTESIAN_POINT ( 'NONE',  ( -0.09139240964747702423, 0.07874015748031500117, -1.981023540891279271E-18 ) ) ;
#11044=ADVANCED_FACE ( 'NONE', ( #26733 ), #26716, .F. ) ;
#11082=CARTESIAN_POINT ( 'NONE',  ( -0.08530183727034104657, 0.03937007874015747977, 0.06819097667594015144 ) ) ;
#11090=CARTESIAN_POINT ( 'NONE',  ( 8.810208661417323492E-17, -4.420669291338583154E-18, 0.000000000000000000 ) ) ;
#11222=PLANE ( 'NONE',  #22678 ) ;
#11389=EDGE_LOOP ( 'NONE', ( #16582, #5201, #22031, #25192, #23159 ) ) ;
#11419=CIRCLE ( 'NONE', #11868, 0.1673228346456692994 ) ;
#11431=CARTESIAN_POINT ( 'NONE',  ( 0.6106000000000000316, -1.355930314960630041E-19, 0.000000000000000000 ) ) ;
#11550=AXIS2_PLACEMENT_3D ( 'NONE', #16861, #19103, #21235 ) ;
#11557=ORIENTED_EDGE ( 'NONE', *, *, #1471, .F. ) ;
#11569=CARTESIAN_POINT ( 'NONE',  ( 0.003937007874015826907, 8.142711329854796413E-18, 0.1023622047244094474 ) ) ;
#11588=AXIS2_PLACEMENT_3D ( 'NONE', #5229, #3665, #7923 ) ;
#11646=VECTOR ( 'NONE', #6555, 39.37007874015748143 ) ;
#11700=EDGE_CURVE ( 'NONE', #13428, #20556, #13788, .T. ) ;
#11705=AXIS2_PLACEMENT_3D ( 'NONE', #18024, #9861, #3061 ) ;
#11769=ORIENTED_EDGE ( 'NONE', *, *, #13508, .T. ) ;
#11808=CARTESIAN_POINT ( 'NONE',  ( -0.07217847769028858107, 0.04546065111729338110, 0.000000000000000000 ) ) ;
#11868=AXIS2_PLACEMENT_3D ( 'NONE', #9762, #18220, #2967 ) ;
#11946=VERTEX_POINT ( 'NONE', #22979 ) ;
#12061=DIRECTION ( 'NONE',  ( 1.000000000000000000, 7.017815000000000124E-18, 0.000000000000000000 ) ) ;
#12144=ORIENTED_EDGE ( 'NONE', *, *, #19914, .T. ) ;
#12165=AXIS2_PLACEMENT_3D ( 'NONE', #9502, #12061, #7400 ) ;
#12273=PRODUCT_DEFINITION_SHAPE ( 'NONE', 'NONE',  #2378 ) ;
#12275=AXIS2_PLACEMENT_3D ( 'NONE', #5534, #14596, #23198 ) ;
#12302=CARTESIAN_POINT ( 'NONE',  ( -0.1968503937007874127, -5.802129921259842692E-18, 0.000000000000000000 ) ) ;
#12312=CARTESIAN_POINT ( 'NONE',  ( 0.6299212598425196763, -1.895600393700787470E-35, 0.000000000000000000 ) ) ;
#12313=CIRCLE ( 'NONE', #1486, 0.1673228346456692994 ) ;
#12431=AXIS2_PLACEMENT_3D ( 'NONE', #12868, #6519, #27721 ) ;
#12453=FACE_OUTER_BOUND ( 'NONE', #4969, .T. ) ;
#12461=DIRECTION ( 'NONE',  ( 0.000000000000000000, -1.000000000000000000, 0.000000000000000000 ) ) ;
#12474=ADVANCED_FACE ( 'NONE', ( #27059 ), #18534, .T. ) ;
#12530=CARTESIAN_POINT ( 'NONE',  ( 0.003937007874015826907, -4.393043307086613241E-18, 0.000000000000000000 ) ) ;
#12568=DIRECTION ( 'NONE',  ( -1.000000000000000000, 0.000000000000000000, 0.000000000000000000 ) ) ;
#12572=CYLINDRICAL_SURFACE ( 'NONE', #8766, 0.1673228346456692994 ) ;
#12702=FACE_OUTER_BOUND ( 'NONE', #15120, .T. ) ;
#12735=CARTESIAN_POINT ( 'NONE',  ( -0.09139240964747703810, 0.07874015748031500117, 0.02109836160874967170 ) ) ;
#12868=CARTESIAN_POINT ( 'NONE',  ( 8.810208661417323492E-17, -4.420669291338583154E-18, 0.000000000000000000 ) ) ;
#12916=CARTESIAN_POINT ( 'NONE',  ( 0.6299212598425196763, 0.07910393700787400617, 1.087052427555504903E-17 ) ) ;
#12930=CARTESIAN_POINT ( 'NONE',  ( -0.1771653543307086520, -5.663984251968503442E-18, 0.000000000000000000 ) ) ;
#12950=ORIENTED_EDGE ( 'NONE', *, *, #9446, .T. ) ;
#12957=ORIENTED_EDGE ( 'NONE', *, *, #23, .F. ) ;
#12986=VERTEX_POINT ( 'NONE', #18868 ) ;
#13003=AXIS2_PLACEMENT_3D ( 'NONE', #13876, #22073, #9772 ) ;
#13072=DIRECTION ( 'NONE',  ( 0.000000000000000000, 1.000000000000000000, 0.000000000000000000 ) ) ;
#13094=VERTEX_POINT ( 'NONE', #14946 ) ;
#13103=ORIENTED_EDGE ( 'NONE', *, *, #5694, .F. ) ;
#13187=CARTESIAN_POINT ( 'NONE',  ( 0.6299212598425196763, -0.07910393700787400617, 0.000000000000000000 ) ) ;
#13197=LINE ( 'NONE', #21827, #17094 ) ;
#13205=FACE_OUTER_BOUND ( 'NONE', #4216, .T. ) ;
#13212=AXIS2_PLACEMENT_3D ( 'NONE', #20785, #14299, #18504 ) ;
#13245=FACE_BOUND ( 'NONE', #19302, .T. ) ;
#13301=VECTOR ( 'NONE', #6737, 39.37007874015748143 ) ;
#13355=LINE ( 'NONE', #9376, #13301 ) ;
#13398=ORIENTED_EDGE ( 'NONE', *, *, #13508, .F. ) ;
#13428=VERTEX_POINT ( 'NONE', #20513 ) ;
#13431=CIRCLE ( 'NONE', #10750, 0.09842519685039370636 ) ;
#13500=EDGE_LOOP ( 'NONE', ( #11557, #17054, #19385, #6074, #21023 ) ) ;
#13504=ORIENTED_EDGE ( 'NONE', *, *, #8464, .F. ) ;
#13508=EDGE_CURVE ( 'NONE', #19742, #19722, #7792, .T. ) ;
#13578=CIRCLE ( 'NONE', #976, 0.01968503937007872254 ) ;
#13641=VERTEX_POINT ( 'NONE', #6667 ) ;
#13658=DIRECTION ( 'NONE',  ( -1.000000000000000000, 0.000000000000000000, 4.051737956723259176E-18 ) ) ;
#13660=CARTESIAN_POINT ( 'NONE',  ( -0.1771653543307086520, -0.1673228346456692994, 2.049113738730807629E-17 ) ) ;
#13676=VERTEX_POINT ( 'NONE', #17394 ) ;
#13788=LINE ( 'NONE', #11808, #26735 ) ;
#13872=EDGE_CURVE ( 'NONE', #25766, #13094, #26749, .T. ) ;
#13876=CARTESIAN_POINT ( 'NONE',  ( 0.003937007874015826907, -4.393043307086613241E-18, 0.000000000000000000 ) ) ;
#13903=ORIENTED_EDGE ( 'NONE', *, *, #9857, .F. ) ;
#13905=LINE ( 'NONE', #27048, #21017 ) ;
#14055=ORIENTED_EDGE ( 'NONE', *, *, #13872, .T. ) ;
#14189=AXIS2_PLACEMENT_3D ( 'NONE', #24170, #19793, #21921 ) ;
#14224=VERTEX_POINT ( 'NONE', #13660 ) ;
#14257=EDGE_LOOP ( 'NONE', ( #19261, #17336, #655, #26262, #20389, #23295 ) ) ;
#14299=DIRECTION ( 'NONE',  ( 1.000000000000000000, 0.000000000000000000, 0.000000000000000000 ) ) ;
#14443=EDGE_CURVE ( 'NONE', #15671, #7941, #20488, .T. ) ;
#14482=CARTESIAN_POINT ( 'NONE',  ( -0.1968503937007874127, 0.000000000000000000, 0.09092130223458683158 ) ) ;
#14499=VERTEX_POINT ( 'NONE', #17944 ) ;
#14523=VECTOR ( 'NONE', #18254, 39.37007874015748143 ) ;
#14586=VERTEX_POINT ( 'NONE', #20939 ) ;
#14596=DIRECTION ( 'NONE',  ( 3.508907999999999048E-18, -0.4999999999999998890, 0.8660254037844388186 ) ) ;
#14613=AXIS2_PLACEMENT_3D ( 'NONE', #24852, #24427, #27827 ) ;
#14639=VECTOR ( 'NONE', #9933, 39.37007874015748854 ) ;
#14779=ORIENTED_EDGE ( 'NONE', *, *, #2141, .T. ) ;
#14809=ADVANCED_FACE ( 'NONE', ( #25883 ), #4411, .F. ) ;
#14814=AXIS2_PLACEMENT_3D ( 'NONE', #12302, #20925, #1569 ) ;
#14863=AXIS2_PLACEMENT_3D ( 'NONE', #8823, #26061, #7122 ) ;
#14908=EDGE_CURVE ( 'NONE', #19722, #19742, #5612, .T. ) ;
#14946=CARTESIAN_POINT ( 'NONE',  ( -0.1771653543307086520, 1.482715313533957208E-17, 0.1673228346456692994 ) ) ;
#15017=CARTESIAN_POINT ( 'NONE',  ( 0.003937007874015826907, -0.09842519685039370636, 1.205361022782828035E-17 ) ) ;
#15120=EDGE_LOOP ( 'NONE', ( #13903, #17075, #27670, #10009, #4760 ) ) ;
#15123=AXIS2_PLACEMENT_3D ( 'NONE', #15533, #15406, #17884 ) ;
#15206=EDGE_CURVE ( 'NONE', #25403, #27013, #4098, .T. ) ;
#15208=CYLINDRICAL_SURFACE ( 'NONE', #27576, 0.1673228346456692994 ) ;
#15227=EDGE_CURVE ( 'NONE', #17614, #19912, #10392, .T. ) ;
#15235=SHAPE_REPRESENTATION_RELATIONSHIP ( 'NONE' , 'NONE' ,  #9188, #24457 ) ;
#15257=FACE_OUTER_BOUND ( 'NONE', #4332, .T. ) ;
#15290=( BOUNDED_CURVE ( )  B_SPLINE_CURVE ( 2, ( #20635, #3234, #5811 ),
 .UNSPECIFIED., .F., .T. ) 
 B_SPLINE_CURVE_WITH_KNOTS ( ( 3, 3 ),
 ( 0.000000000000000000, 0.2336872276155829986 ),
 .UNSPECIFIED. ) 
 CURVE ( )  GEOMETRIC_REPRESENTATION_ITEM ( )  RATIONAL_B_SPLINE_CURVE ( ( 1.000000000000000000, 1.154700538379243913, 1.000000000000000000 ) ) 
 REPRESENTATION_ITEM ( '' )  ) ;
#15298=CARTESIAN_POINT ( 'NONE',  ( 0.6202606299212598540, -6.779653543307085645E-20, 0.000000000000000000 ) ) ;
#15333=CARTESIAN_POINT ( 'NONE',  ( -0.08530183727034117147, -0.03937007874015755610, -0.06819097667594038736 ) ) ;
#15400=CARTESIAN_POINT ( 'NONE',  ( -0.1968503937007874127, 0.1291220684401279684, 0.000000000000000000 ) ) ;
#15406=DIRECTION ( 'NONE',  ( -1.000000000000000000, 0.000000000000000000, 0.000000000000000000 ) ) ;
#15435=AXIS2_PLACEMENT_3D ( 'NONE', #24368, #24924, #5584 ) ;
#15457=LINE ( 'NONE', #17417, #11646 ) ;
#15478=AXIS2_PLACEMENT_3D ( 'NONE', #20670, #24899, #7533 ) ;
#15533=CARTESIAN_POINT ( 'NONE',  ( -0.1771653543307086520, -5.663984251968503442E-18, 0.000000000000000000 ) ) ;
#15671=VERTEX_POINT ( 'NONE', #15017 ) ;
#15686=CARTESIAN_POINT ( 'NONE',  ( 0.3543307086614173040, -1.934043700787401319E-18, 0.000000000000000000 ) ) ;
#15712=CARTESIAN_POINT ( 'NONE',  ( -0.1968503937007874127, 0.07874015748031495954, -0.04546065111729338803 ) ) ;
#15741=ORIENTED_EDGE ( 'NONE', *, *, #17788, .T. ) ;
#15769=CONICAL_SURFACE ( 'NONE', #11705, 0.04546065111729338803, 1.047197549999998811 ) ;
#15936=CONICAL_SURFACE ( 'NONE', #5095, 0.04546065111729338803, 1.047197549999998811 ) ;
#15992=ORIENTED_EDGE ( 'NONE', *, *, #26466, .T. ) ;
#16017=ORIENTED_EDGE ( 'NONE', *, *, #20971, .F. ) ;
#16072=ORIENTED_EDGE ( 'NONE', *, *, #5952, .F. ) ;
#16086=CARTESIAN_POINT ( 'NONE',  ( 8.353478384051541640E-17, -4.420672499999999463E-18, -0.1023622047244094474 ) ) ;
#16101=DIRECTION ( 'NONE',  ( -1.000000000000000000, 0.000000000000000000, 0.000000000000000000 ) ) ;
#16130=ORIENTED_EDGE ( 'NONE', *, *, #6942, .T. ) ;
#16239=TOROIDAL_SURFACE ( 'NONE', #12165, 0.1023622047244094474, 0.003937007874015747977 ) ;
#16240=VECTOR ( 'NONE', #4054, 39.37007874015748143 ) ;
#16350=FACE_OUTER_BOUND ( 'NONE', #20942, .T. ) ;
#16436=CARTESIAN_POINT ( 'NONE',  ( -0.1968503937007874127, -3.496765354330708585E-17, -0.09092130223458683158 ) ) ;
#16508=LINE ( 'NONE', #16798, #9021 ) ;
#16553=PRODUCT ( 'ISO 4762 M5x16 Socket Head Cap Screw', 'ISO 4762 M5x16 Socket Head Cap Screw', '', ( #2873 ) ) ;
#16582=ORIENTED_EDGE ( 'NONE', *, *, #13872, .F. ) ;
#16780=AXIS2_PLACEMENT_3D ( 'NONE', #10490, #27607, #25483 ) ;
#16798=CARTESIAN_POINT ( 'NONE',  ( 0.6202606299212598540, -0.08876456692913387014, 0.000000000000000000 ) ) ;
#16815=CARTESIAN_POINT ( 'NONE',  ( -0.09842519685039370636, -0.07874015748031495954, -0.04546065111729338803 ) ) ;
#16861=CARTESIAN_POINT ( 'NONE',  ( 0.6106000000000000316, -1.355930314960630041E-19, 0.000000000000000000 ) ) ;
#16990=ADVANCED_FACE ( 'NONE', ( #1197 ), #16239, .F. ) ;
#16994=CIRCLE ( 'NONE', #22386, 0.1673228346456692994 ) ;
#17021=COLOUR_RGB ( '', 0.72549020, 0.75294118, 0.79215686) ;
#17054=ORIENTED_EDGE ( 'NONE', *, *, #383, .F. ) ;
#17075=ORIENTED_EDGE ( 'NONE', *, *, #6770, .F. ) ;
#17094=VECTOR ( 'NONE', #375, 39.37007874015748854 ) ;
#17125=DIRECTION ( 'NONE',  ( 1.000000000000000000, 0.000000000000000000, 0.000000000000000000 ) ) ;
#17131=CARTESIAN_POINT ( 'NONE',  ( -0.09842519685039370636, -0.07874015748031495954, -0.04546065111729338803 ) ) ;
#17256=CARTESIAN_POINT ( 'NONE',  ( 0.003937007874015826907, -4.393043307086613241E-18, 0.000000000000000000 ) ) ;
#17324=FACE_OUTER_BOUND ( 'NONE', #14257, .T. ) ;
#17336=ORIENTED_EDGE ( 'NONE', *, *, #20971, .T. ) ;
#17352=VECTOR ( 'NONE', #3813, 39.37007874015748854 ) ;
#17378=VERTEX_POINT ( 'NONE', #15712 ) ;
#17392=FACE_OUTER_BOUND ( 'NONE', #27114, .T. ) ;
#17394=CARTESIAN_POINT ( 'NONE',  ( 0.6106000000000000316, -0.09842519683305382683, 0.000000000000000000 ) ) ;
#17396=DIRECTION ( 'NONE',  ( 0.000000000000000000, -1.000000000000000000, 0.000000000000000000 ) ) ;
#17417=CARTESIAN_POINT ( 'NONE',  ( -0.1968503937007874127, 4.336421259842520449E-17, 0.09092130223458683158 ) ) ;
#17462=AXIS2_PLACEMENT_3D ( 'NONE', #22469, #1558, #3230 ) ;
#17489=EDGE_CURVE ( 'NONE', #25766, #13641, #26964, .T. ) ;
#17529=DIRECTION ( 'NONE',  ( 0.000000000000000000, -1.000000000000000000, 0.000000000000000000 ) ) ;
#17546=VECTOR ( 'NONE', #26040, 39.37007874015748143 ) ;
#17578=CARTESIAN_POINT ( 'NONE',  ( 0.6202606299212598540, 0.08876456692913387014, 1.087052427674648014E-17 ) ) ;
#17590=VERTEX_POINT ( 'NONE', #24157 ) ;
#17614=VERTEX_POINT ( 'NONE', #8626 ) ;
#17716=DIRECTION ( 'NONE',  ( 1.000000000000000000, 7.017815000000000124E-18, 0.000000000000000000 ) ) ;
#17764=CIRCLE ( 'NONE', #2425, 0.09842519685039370636 ) ;
#17773=LINE ( 'NONE', #10871, #25586 ) ;
#17788=EDGE_CURVE ( 'NONE', #13676, #14586, #13431, .T. ) ;
#17834=CARTESIAN_POINT ( 'NONE',  ( -0.09842519685039370636, 0.07874015748031495954, 0.04546065111729331171 ) ) ;
#17835=VECTOR ( 'NONE', #27626, 39.37007874015748143 ) ;
#17883=DIRECTION ( 'NONE',  ( 0.000000000000000000, -1.000000000000000000, 0.000000000000000000 ) ) ;
#17884=DIRECTION ( 'NONE',  ( 0.000000000000000000, -1.000000000000000000, 0.000000000000000000 ) ) ;
#17944=CARTESIAN_POINT ( 'NONE',  ( -0.1968503937007874127, -0.07874015748031495954, 0.04546065111729338803 ) ) ;
#18024=CARTESIAN_POINT ( 'NONE',  ( -0.07217847769028858107, -4.927204724409449161E-18, 0.000000000000000000 ) ) ;
#18115=ORIENTED_EDGE ( 'NONE', *, *, #14908, .F. ) ;
#18124=AXIS2_PLACEMENT_3D ( 'NONE', #3723, #18977, #1747 ) ;
#18194=VERTEX_POINT ( 'NONE', #1504 ) ;
#18220=DIRECTION ( 'NONE',  ( -1.000000000000000000, 0.000000000000000000, 0.000000000000000000 ) ) ;
#18254=DIRECTION ( 'NONE',  ( 1.000000000000000000, 0.000000000000000000, 0.000000000000000000 ) ) ;
#18266=SHAPE_DEFINITION_REPRESENTATION ( #12273, #9188 ) ;
#18275=SURFACE_STYLE_FILL_AREA ( #20133 ) ;
#18382=CONICAL_SURFACE ( 'NONE', #8493, 0.08876456692913387014, 0.7853981624999977207 ) ;
#18504=DIRECTION ( 'NONE',  ( 0.000000000000000000, 1.000000000000000000, 0.000000000000000000 ) ) ;
#18534=TOROIDAL_SURFACE ( 'NONE', #15435, 0.1476377952755905387, 0.01968503937007873988 ) ;
#18749=ADVANCED_FACE ( 'NONE', ( #5495 ), #15769, .F. ) ;
#18856=ORIENTED_EDGE ( 'NONE', *, *, #19680, .F. ) ;
#18868=CARTESIAN_POINT ( 'NONE',  ( -0.09842519685039370636, 2.800920866141732248E-17, 0.09092130223458683158 ) ) ;
#18954=CARTESIAN_POINT ( 'NONE',  ( -0.1968503937007874127, 0.07874015748031495954, 0.04546065111729331171 ) ) ;
#18977=DIRECTION ( 'NONE',  ( 1.000000000000000000, 0.000000000000000000, 0.000000000000000000 ) ) ;
#19058=CARTESIAN_POINT ( 'NONE',  ( -0.1968503937007874127, 0.07874015748031495954, 0.04546065111729331171 ) ) ;
#19074=EDGE_CURVE ( 'NONE', #7850, #4078, #17773, .T. ) ;
#19103=DIRECTION ( 'NONE',  ( 1.000000000000000000, 0.000000000000000000, 0.000000000000000000 ) ) ;
#19107=CLOSED_SHELL ( 'NONE', ( #11044, #10180, #26396, #25386, #7661, #203, #18749, #8747, #5433, #1568, #14809, #4837, #21560, #934, #23805, #12474, #9345, #4807, #7085, #23505, #16990 ) ) ;
#19261=ORIENTED_EDGE ( 'NONE', *, *, #11700, .F. ) ;
#19275=( BOUNDED_CURVE ( )  B_SPLINE_CURVE ( 2, ( #5340, #26958, #24678 ),
 .UNSPECIFIED., .F., .T. ) 
 B_SPLINE_CURVE_WITH_KNOTS ( ( 3, 3 ),
 ( 0.1168436138077912356, 0.2336872276155829986 ),
 .UNSPECIFIED. ) 
 CURVE ( )  GEOMETRIC_REPRESENTATION_ITEM ( )  RATIONAL_B_SPLINE_CURVE ( ( 1.077350269189625953, 1.077350269189626175, 1.000000000000000000 ) ) 
 REPRESENTATION_ITEM ( '' )  ) ;
#19302=EDGE_LOOP ( 'NONE', ( #22684, #25305 ) ) ;
#19344=CARTESIAN_POINT ( 'NONE',  ( -0.09842519685039370636, 0.07874015748031495954, -0.04546065111729338803 ) ) ;
#19385=ORIENTED_EDGE ( 'NONE', *, *, #4766, .F. ) ;
#19387=FACE_OUTER_BOUND ( 'NONE', #25824, .T. ) ;
#19420=CARTESIAN_POINT ( 'NONE',  ( -0.09842519685039370636, 0.1673228346456692994, 0.000000000000000000 ) ) ;
#19432=CARTESIAN_POINT ( 'NONE',  ( 0.6299212598425196763, 0.04921259842519685318, 0.000000000000000000 ) ) ;
#19487=DIRECTION ( 'NONE',  ( 0.000000000000000000, 0.8660254037844385966, -0.4999999999999998335 ) ) ;
#19589=VERTEX_POINT ( 'NONE', #10377 ) ;
#19591=ORIENTED_EDGE ( 'NONE', *, *, #6447, .T. ) ;
#19615=ORIENTED_EDGE ( 'NONE', *, *, #24344, .F. ) ;
#19660=DIRECTION ( 'NONE',  ( 0.000000000000000000, -1.000000000000000000, 0.000000000000000000 ) ) ;
#19680=EDGE_CURVE ( 'NONE', #21206, #20489, #8680, .T. ) ;
#19684=CARTESIAN_POINT ( 'NONE',  ( -0.09842519685039370636, -0.1673228346456692994, 2.049113738730807629E-17 ) ) ;
#19722=VERTEX_POINT ( 'NONE', #12916 ) ;
#19742=VERTEX_POINT ( 'NONE', #13187 ) ;
#19788=ORIENTED_EDGE ( 'NONE', *, *, #14443, .T. ) ;
#19793=DIRECTION ( 'NONE',  ( -1.000000000000000000, 0.000000000000000000, 0.000000000000000000 ) ) ;
#19818=VECTOR ( 'NONE', #616, 39.37007874015748143 ) ;
#19821=DIRECTION ( 'NONE',  ( 0.000000000000000000, -1.000000000000000000, 0.000000000000000000 ) ) ;
#19839=ORIENTED_EDGE ( 'NONE', *, *, #6447, .F. ) ;
#19912=VERTEX_POINT ( 'NONE', #4002 ) ;
#19914=EDGE_CURVE ( 'NONE', #14586, #13676, #7504, .T. ) ;
#19961=EDGE_CURVE ( 'NONE', #13094, #21206, #16994, .T. ) ;
#19983=CARTESIAN_POINT ( 'NONE',  ( -0.1968503937007874127, 0.07874015748031495954, 0.04546065111729331171 ) ) ;
#19998=( NAMED_UNIT ( * ) PLANE_ANGLE_UNIT ( ) SI_UNIT ( $, .RADIAN. ) ) ;
#20057=DIRECTION ( 'NONE',  ( 0.000000000000000000, 1.000000000000000000, 0.000000000000000000 ) ) ;
#20093=DIRECTION ( 'NONE',  ( 0.000000000000000000, 1.000000000000000000, 0.000000000000000000 ) ) ;
#20133=FILL_AREA_STYLE ('',( #9675 ) ) ;
#20333=DIRECTION ( 'NONE',  ( 1.000000000000000000, 0.000000000000000000, 0.000000000000000000 ) ) ;
#20337=CARTESIAN_POINT ( 'NONE',  ( 0.003937007874015826907, -4.406857903543305967E-18, -0.09842519685039370636 ) ) ;
#20389=ORIENTED_EDGE ( 'NONE', *, *, #10995, .T. ) ;
#20488=CIRCLE ( 'NONE', #643, 0.09842519685039370636 ) ;
#20489=VERTEX_POINT ( 'NONE', #3373 ) ;
#20497=VECTOR ( 'NONE', #3955, 39.37007874015748143 ) ;
#20513=CARTESIAN_POINT ( 'NONE',  ( -0.04593175845765267579, -4.927204724409449161E-18, 0.000000000000000000 ) ) ;
#20556=VERTEX_POINT ( 'NONE', #3521 ) ;
#20590=CARTESIAN_POINT ( 'NONE',  ( -0.1968503937007874127, -1.676732283464567127E-17, -0.09092130223458683158 ) ) ;
#20635=CARTESIAN_POINT ( 'NONE',  ( -0.09842519685039370636, -0.07874015748031495954, 0.04546065111729338803 ) ) ;
#20670=CARTESIAN_POINT ( 'NONE',  ( 0.003937007874015826907, -4.393043307086613241E-18, 0.000000000000000000 ) ) ;
#20671=ORIENTED_EDGE ( 'NONE', *, *, #1078, .T. ) ;
#20699=ORIENTED_EDGE ( 'NONE', *, *, #24344, .T. ) ;
#20740=ORIENTED_EDGE ( 'NONE', *, *, #5952, .T. ) ;
#20753=AXIS2_PLACEMENT_3D ( 'NONE', #6762, #23727, #26238 ) ;
#20785=CARTESIAN_POINT ( 'NONE',  ( 0.3543307086614173040, -1.934043700787401319E-18, 0.000000000000000000 ) ) ;
#20863=EDGE_LOOP ( 'NONE', ( #10835, #14055, #5247, #20671, #6499 ) ) ;
#20893=EDGE_CURVE ( 'NONE', #23520, #22723, #27479, .T. ) ;
#20925=DIRECTION ( 'NONE',  ( 1.000000000000000000, 0.000000000000000000, 0.000000000000000000 ) ) ;
#20939=CARTESIAN_POINT ( 'NONE',  ( 0.6106000000000000316, 0.09842519683305382683, 1.205361022570475770E-17 ) ) ;
#20942=EDGE_LOOP ( 'NONE', ( #8718, #9716, #19615, #19839 ) ) ;
#20950=ORIENTED_EDGE ( 'NONE', *, *, #7954, .F. ) ;
#20971=EDGE_CURVE ( 'NONE', #13428, #7191, #13197, .T. ) ;
#21017=VECTOR ( 'NONE', #7696, 39.37007874015748143 ) ;
#21023=ORIENTED_EDGE ( 'NONE', *, *, #17788, .F. ) ;
#21058=ORIENTED_EDGE ( 'NONE', *, *, #9079, .T. ) ;
#21122=CARTESIAN_POINT ( 'NONE',  ( -0.09842519685039370636, 0.07874015748031495954, -0.04546065111729338803 ) ) ;
#21192=CARTESIAN_POINT ( 'NONE',  ( -0.08530183727034107433, 0.03937007874015742426, -0.06819097667594002654 ) ) ;
#21206=VERTEX_POINT ( 'NONE', #23378 ) ;
#21235=DIRECTION ( 'NONE',  ( 0.000000000000000000, -1.000000000000000000, 0.000000000000000000 ) ) ;
#21315=VERTEX_POINT ( 'NONE', #8789 ) ;
#21335=DIRECTION ( 'NONE',  ( 1.000000000000000000, 0.000000000000000000, 0.000000000000000000 ) ) ;
#21516=CARTESIAN_POINT ( 'NONE',  ( 0.6202606299212598540, -6.779653543307085645E-20, 0.000000000000000000 ) ) ;
#21560=ADVANCED_FACE ( 'NONE', ( #24862 ), #24716, .F. ) ;
#21587=CIRCLE ( 'NONE', #13003, 0.09842519685039370636 ) ;
#21626=CARTESIAN_POINT ( 'NONE',  ( -0.1771653543307086520, -5.663984251968503442E-18, -0.1673228346456692994 ) ) ;
#21665=DIRECTION ( 'NONE',  ( 1.000000000000000000, 0.000000000000000000, 0.000000000000000000 ) ) ;
#21666=ORIENTED_EDGE ( 'NONE', *, *, #3710, .T. ) ;
#21706=VECTOR ( 'NONE', #9936, 39.37007874015748854 ) ;
#21744=LINE ( 'NONE', #25426, #20497 ) ;
#21757=CARTESIAN_POINT ( 'NONE',  ( -0.1968503937007874127, 5.332515748031495785E-18, 0.09092130223458683158 ) ) ;
#21784=DIRECTION ( 'NONE',  ( 0.000000000000000000, -1.000000000000000000, 0.000000000000000000 ) ) ;
#21788=EDGE_CURVE ( 'NONE', #13641, #27702, #13578, .T. ) ;
#21827=CARTESIAN_POINT ( 'NONE',  ( -0.07217847769028858107, -0.04546065111729339497, -5.567324087794789421E-18 ) ) ;
#21842=AXIS2_PLACEMENT_3D ( 'NONE', #18954, #2004, #17125 ) ;
#21880=PLANE ( 'NONE',  #9391 ) ;
#21921=DIRECTION ( 'NONE',  ( 0.000000000000000000, -1.000000000000000000, 0.000000000000000000 ) ) ;
#21926=MANIFOLD_SOLID_BREP ( 'ISO 4762 M5x16 Socket Head Cap Screw', #19107 ) ;
#21990=ORIENTED_EDGE ( 'NONE', *, *, #3710, .F. ) ;
#22031=ORIENTED_EDGE ( 'NONE', *, *, #21788, .T. ) ;
#22073=DIRECTION ( 'NONE',  ( -1.000000000000000000, 0.000000000000000000, 0.000000000000000000 ) ) ;
#22175=CYLINDRICAL_SURFACE ( 'NONE', #2840, 0.09842519685039370636 ) ;
#22253=SURFACE_STYLE_USAGE ( .BOTH. , #5299 ) ;
#22365=( NAMED_UNIT ( * ) PLANE_ANGLE_UNIT ( ) SI_UNIT ( $, .RADIAN. ) ) ;
#22386=AXIS2_PLACEMENT_3D ( 'NONE', #9923, #6263, #22785 ) ;
#22469=CARTESIAN_POINT ( 'NONE',  ( -0.1968503937007874127, -1.676732283464567127E-17, -0.09092130223458683158 ) ) ;
#22538=LENGTH_MEASURE_WITH_UNIT ( LENGTH_MEASURE( 0.02539999999999999897 ), #3018 ) ;
#22595=APPLICATION_CONTEXT ( 'automotive_design' ) ;
#22678=AXIS2_PLACEMENT_3D ( 'NONE', #19432, #2196, #9094 ) ;
#22684=ORIENTED_EDGE ( 'NONE', *, *, #27335, .F. ) ;
#22723=VERTEX_POINT ( 'NONE', #16086 ) ;
#22784=CIRCLE ( 'NONE', #12431, 0.1023622047244094474 ) ;
#22785=DIRECTION ( 'NONE',  ( 0.000000000000000000, -1.000000000000000000, 0.000000000000000000 ) ) ;
#22881=DIRECTION ( 'NONE',  ( -0.7071067818211409506, -0.7071067805519539728, 0.000000000000000000 ) ) ;
#22979=CARTESIAN_POINT ( 'NONE',  ( 8.741913385826771462E-17, -0.1673228346456692994, 2.049113738730807629E-17 ) ) ;
#23023=CIRCLE ( 'NONE', #472, 0.1673228346456692994 ) ;
#23036=CARTESIAN_POINT ( 'NONE',  ( -0.09842519685039370636, -1.570035826771653483E-17, -0.09092130223458683158 ) ) ;
#23159=ORIENTED_EDGE ( 'NONE', *, *, #10017, .T. ) ;
#23198=DIRECTION ( 'NONE',  ( -1.000000000000000000, -7.017815999999999636E-18, 0.000000000000000000 ) ) ;
#23233=ORIENTED_EDGE ( 'NONE', *, *, #3626, .T. ) ;
#23295=ORIENTED_EDGE ( 'NONE', *, *, #440, .T. ) ;
#23378=CARTESIAN_POINT ( 'NONE',  ( -0.1771653543307086520, 0.1673228346456692994, 0.000000000000000000 ) ) ;
#23416=CARTESIAN_POINT ( 'NONE',  ( -0.09842519685039370636, -5.111401574803149519E-18, 0.000000000000000000 ) ) ;
#23505=ADVANCED_FACE ( 'NONE', ( #2945 ), #22175, .T. ) ;
#23520=VERTEX_POINT ( 'NONE', #20337 ) ;
#23613=CIRCLE ( 'NONE', #18124, 0.1476377952755905387 ) ;
#23727=DIRECTION ( 'NONE',  ( 1.000000000000000000, 0.000000000000000000, 0.000000000000000000 ) ) ;
#23805=ADVANCED_FACE ( 'NONE', ( #25978, #15257 ), #23869, .T. ) ;
#23864=FACE_OUTER_BOUND ( 'NONE', #10764, .T. ) ;
#23869=PLANE ( 'NONE',  #26754 ) ;
#24037=CARTESIAN_POINT ( 'NONE',  ( -0.09842519685039370636, -0.07874015748031495954, 0.04546065111729338803 ) ) ;
#24081=DIRECTION ( 'NONE',  ( 0.000000000000000000, -1.000000000000000000, 0.000000000000000000 ) ) ;
#24083=CARTESIAN_POINT ( 'NONE',  ( -0.1968503937007874127, -0.07874015748031495954, -0.04546065111729331171 ) ) ;
#24137=EDGE_LOOP ( 'NONE', ( #24608, #10142, #13504, #18856, #5837 ) ) ;
#24157=CARTESIAN_POINT ( 'NONE',  ( 8.353478384051541640E-17, 8.115082136941410961E-18, 0.1023622047244094474 ) ) ;
#24170=CARTESIAN_POINT ( 'NONE',  ( 0.6299212598425196763, -1.895600393700787470E-35, 0.000000000000000000 ) ) ;
#24206=EDGE_CURVE ( 'NONE', #830, #7850, #25421, .T. ) ;
#24344=EDGE_CURVE ( 'NONE', #4078, #17378, #9650, .T. ) ;
#24355=DIRECTION ( 'NONE',  ( 0.000000000000000000, 1.000000000000000000, 0.000000000000000000 ) ) ;
#24367=DIRECTION ( 'NONE',  ( -3.508908000000002129E-18, 0.5000000000000003331, 0.8660254037844384856 ) ) ;
#24368=CARTESIAN_POINT ( 'NONE',  ( -0.1771653543307086520, -5.663984251968503442E-18, 0.000000000000000000 ) ) ;
#24427=DIRECTION ( 'NONE',  ( -7.017815000000000124E-18, 1.000000000000000000, -1.224646799147353207E-16 ) ) ;
#24457=ADVANCED_BREP_SHAPE_REPRESENTATION ( 'ISO 4762 M5x16 Socket Head Cap Screw', ( #21926, #11588 ), #3473 ) ;
#24555=CARTESIAN_POINT ( 'NONE',  ( -0.1771653543307086520, -5.663984251968503442E-18, 0.000000000000000000 ) ) ;
#24572=TOROIDAL_SURFACE ( 'NONE', #10584, 0.1476377952755905387, 0.01968503937007873988 ) ;
#24608=ORIENTED_EDGE ( 'NONE', *, *, #10017, .F. ) ;
#24651=DIRECTION ( 'NONE',  ( -0.5000000010362850578, 0.8660254031861391866, 0.000000000000000000 ) ) ;
#24661=DIRECTION ( 'NONE',  ( 0.000000000000000000, 0.000000000000000000, 1.000000000000000000 ) ) ;
#24678=CARTESIAN_POINT ( 'NONE',  ( -0.09842519685039370636, 0.07874015748031495954, -0.04546065111729338803 ) ) ;
#24716=PLANE ( 'NONE',  #17462 ) ;
#24771=DIRECTION ( 'NONE',  ( 1.000000000000000000, 0.000000000000000000, 0.000000000000000000 ) ) ;
#24789=DIMENSIONAL_EXPONENTS ( 1.000000000000000000, 0.000000000000000000, 0.000000000000000000, 0.000000000000000000, 0.000000000000000000, 0.000000000000000000, 0.000000000000000000 ) ;
#24852=CARTESIAN_POINT ( 'NONE',  ( -0.1771653543307086520, 1.241643108977391477E-17, 0.1476377952755905387 ) ) ;
#24862=FACE_OUTER_BOUND ( 'NONE', #2619, .T. ) ;
#24899=DIRECTION ( 'NONE',  ( 1.000000000000000000, 7.017815000000000124E-18, 0.000000000000000000 ) ) ;
#24913=AXIS2_PLACEMENT_3D ( 'NONE', #11569, #569, #5211 ) ;
#24918=PRODUCT_DEFINITION_CONTEXT ( 'detailed design', #5484, 'design' ) ;
#24924=DIRECTION ( 'NONE',  ( 1.000000000000000000, 7.017815000000000124E-18, 0.000000000000000000 ) ) ;
#24974=ORIENTED_EDGE ( 'NONE', *, *, #7954, .T. ) ;
#25192=ORIENTED_EDGE ( 'NONE', *, *, #6770, .T. ) ;
#25305=ORIENTED_EDGE ( 'NONE', *, *, #25706, .F. ) ;
#25323=ORIENTED_EDGE ( 'NONE', *, *, #2141, .F. ) ;
#25368=ORIENTED_EDGE ( 'NONE', *, *, #15227, .T. ) ;
#25386=ADVANCED_FACE ( 'NONE', ( #8697 ), #24572, .T. ) ;
#25395=EDGE_LOOP ( 'NONE', ( #7500, #26218, #21990, #1387, #25507 ) ) ;
#25403=VERTEX_POINT ( 'NONE', #19983 ) ;
#25421=LINE ( 'NONE', #3952, #26794 ) ;
#25426=CARTESIAN_POINT ( 'NONE',  ( -0.09842519685039370636, -0.07874015748031495954, 0.04546065111729331171 ) ) ;
#25483=DIRECTION ( 'NONE',  ( 0.000000000000000000, 1.000000000000000000, 0.000000000000000000 ) ) ;
#25507=ORIENTED_EDGE ( 'NONE', *, *, #26490, .F. ) ;
#25513=ORIENTED_EDGE ( 'NONE', *, *, #19914, .F. ) ;
#25515=DIRECTION ( 'NONE',  ( 1.000000000000000000, 0.000000000000000000, 0.000000000000000000 ) ) ;
#25586=VECTOR ( 'NONE', #19487, 39.37007874015748854 ) ;
#25596=DIRECTION ( 'NONE',  ( -1.000000000000000000, 0.000000000000000000, 0.000000000000000000 ) ) ;
#25706=EDGE_CURVE ( 'NONE', #17590, #22723, #22784, .T. ) ;
#25751=DIRECTION ( 'NONE',  ( -1.000000000000000000, 0.000000000000000000, 0.000000000000000000 ) ) ;
#25766=VERTEX_POINT ( 'NONE', #8903 ) ;
#25824=EDGE_LOOP ( 'NONE', ( #11769, #4641, #12144, #207 ) ) ;
#25838=CIRCLE ( 'NONE', #24913, 0.003937007874015741038 ) ;
#25883=FACE_OUTER_BOUND ( 'NONE', #1391, .T. ) ;
#25930=CIRCLE ( 'NONE', #15123, 0.1673228346456692994 ) ;
#25978=FACE_BOUND ( 'NONE', #5765, .T. ) ;
#26040=DIRECTION ( 'NONE',  ( 0.000000000000000000, 0.000000000000000000, -1.000000000000000000 ) ) ;
#26061=DIRECTION ( 'NONE',  ( 7.017815000000000124E-18, -1.000000000000000000, 0.000000000000000000 ) ) ;
#26090=( NAMED_UNIT ( * ) SI_UNIT ( $, .STERADIAN. ) SOLID_ANGLE_UNIT ( ) ) ;
#26159=CARTESIAN_POINT ( 'NONE',  ( -0.09139240964747710749, -0.07874015748031500117, -1.188614124534770567E-17 ) ) ;
#26191=DIRECTION ( 'NONE',  ( -0.7071067818211409506, 0.7071067805519539728, 8.659560554583403090E-17 ) ) ;
#26214=CARTESIAN_POINT ( 'NONE',  ( -0.1968503937007874127, -1.381459842519685169E-18, 0.09092130223458683158 ) ) ;
#26218=ORIENTED_EDGE ( 'NONE', *, *, #24206, .T. ) ;
#26238=DIRECTION ( 'NONE',  ( 0.000000000000000000, 1.000000000000000000, 0.000000000000000000 ) ) ;
#26262=ORIENTED_EDGE ( 'NONE', *, *, #26620, .T. ) ;
#26368=EDGE_CURVE ( 'NONE', #19589, #25403, #13905, .T. ) ;
#26396=ADVANCED_FACE ( 'NONE', ( #19387 ), #9737, .T. ) ;
#26466=EDGE_CURVE ( 'NONE', #830, #7191, #26806, .T. ) ;
#26490=EDGE_CURVE ( 'NONE', #7191, #18194, #9698, .T. ) ;
#26594=ORIENTED_EDGE ( 'NONE', *, *, #3626, .F. ) ;
#26620=EDGE_CURVE ( 'NONE', #18194, #12986, #15290, .T. ) ;
#26632=ORIENTED_EDGE ( 'NONE', *, *, #15206, .F. ) ;
#26647=DIRECTION ( 'NONE',  ( -3.508907999999997507E-18, 0.4999999999999998890, -0.8660254037844388186 ) ) ;
#26716=TOROIDAL_SURFACE ( 'NONE', #15478, 0.1023622047244094474, 0.003937007874015747977 ) ;
#26733=FACE_OUTER_BOUND ( 'NONE', #6466, .T. ) ;
#26735=VECTOR ( 'NONE', #24651, 39.37007874015748854 ) ;
#26749=CIRCLE ( 'NONE', #14613, 0.01968503937007875723 ) ;
#26754=AXIS2_PLACEMENT_3D ( 'NONE', #15400, #5175, #24661 ) ;
#26793=CARTESIAN_POINT ( 'NONE',  ( -0.1968503937007874127, 0.07874015748031495954, -0.04546065111729338803 ) ) ;
#26794=VECTOR ( 'NONE', #12568, 39.37007874015748143 ) ;
#26806=( BOUNDED_CURVE ( )  B_SPLINE_CURVE ( 2, ( #17131, #6677, #4550 ),
 .UNSPECIFIED., .F., .T. ) 
 B_SPLINE_CURVE_WITH_KNOTS ( ( 3, 3 ),
 ( 0.000000000000000000, 0.1168436138077914160 ),
 .UNSPECIFIED. ) 
 CURVE ( )  GEOMETRIC_REPRESENTATION_ITEM ( )  RATIONAL_B_SPLINE_CURVE ( ( 1.000000000000000000, 1.077350269189623067, 1.077350269189623067 ) ) 
 REPRESENTATION_ITEM ( '' )  ) ;
#26824=DIRECTION ( 'NONE',  ( 0.000000000000000000, -1.000000000000000000, 0.000000000000000000 ) ) ;
#26915=PRESENTATION_STYLE_ASSIGNMENT (( #22253 ) ) ;
#26958=CARTESIAN_POINT ( 'NONE',  ( -0.09139240964747699647, 0.07874015748031500117, -0.02109836160874975844 ) ) ;
#26964=CIRCLE ( 'NONE', #14814, 0.1476377952755905387 ) ;
#27013=VERTEX_POINT ( 'NONE', #21757 ) ;
#27045=LINE ( 'NONE', #1058, #14523 ) ;
#27048=CARTESIAN_POINT ( 'NONE',  ( -0.09842519685039370636, 0.07874015748031495954, 0.04546065111729331171 ) ) ;
#27059=FACE_OUTER_BOUND ( 'NONE', #11389, .T. ) ;
#27114=EDGE_LOOP ( 'NONE', ( #12957, #930, #16130, #15741 ) ) ;
#27315=ORIENTED_EDGE ( 'NONE', *, *, #383, .T. ) ;
#27335=EDGE_CURVE ( 'NONE', #22723, #17590, #8417, .T. ) ;
#27446=ORIENTED_EDGE ( 'NONE', *, *, #9584, .F. ) ;
#27479=CIRCLE ( 'NONE', #14863, 0.003937007874015747977 ) ;
#27576=AXIS2_PLACEMENT_3D ( 'NONE', #23416, #25515, #13072 ) ;
#27577=CYLINDRICAL_SURFACE ( 'NONE', #13212, 0.09842519685039370636 ) ;
#27607=DIRECTION ( 'NONE',  ( 1.000000000000000000, 0.000000000000000000, 0.000000000000000000 ) ) ;
#27626=DIRECTION ( 'NONE',  ( -1.000000000000000000, 0.000000000000000000, 0.000000000000000000 ) ) ;
#27645=FACE_OUTER_BOUND ( 'NONE', #24137, .T. ) ;
#27670=ORIENTED_EDGE ( 'NONE', *, *, #1078, .F. ) ;
#27702=VERTEX_POINT ( 'NONE', #21626 ) ;
#27721=DIRECTION ( 'NONE',  ( 0.000000000000000000, -1.000000000000000000, 0.000000000000000000 ) ) ;
#27827=DIRECTION ( 'NONE',  ( 0.000000000000000000, 1.224646799147352221E-16, 1.000000000000000000 ) ) ;
#27853=STYLED_ITEM ( 'NONE', ( #26915 ), #21926 ) ;
#27975=CARTESIAN_POINT ( '', ( 0.0, 0.0, 0.0 ) ) ;
#27976=DIRECTION ( '', ( 0.0, 0.0, 1.0 ) ) ;
#27977=DIRECTION ( '', ( 1.0, 0.0, 0.0 ) ) ;
#27978=AXIS2_PLACEMENT_3D ( '', #27975, #27976, #27977 ) ;
#27988=CARTESIAN_POINT ( '', ( 0.0, 0.0, 0.0 ) ) ;
#27989=DIRECTION ( '', ( 0.0, 0.0, 1.0 ) ) ;
#27990=DIRECTION ( '', ( 1.0, 0.0, 0.0 ) ) ;
#27991=AXIS2_PLACEMENT_3D ( '', #27988, #27989, #27990 ) ;
#28001=CARTESIAN_POINT ( '', ( 0.0, 0.0, 0.0 ) ) ;
#28002=DIRECTION ( '', ( 0.0, 0.0, 1.0 ) ) ;
#28003=DIRECTION ( '', ( 1.0, 0.0, 0.0 ) ) ;
#28004=AXIS2_PLACEMENT_3D ( '', #28001, #28002, #28003 ) ;
ENDSEC;
END-ISO-10303-21;
